ISO-10303-21;
HEADER;
/* Generated by software containing ST-Developer
 * from STEP Tools, Inc. (www.steptools.com) 
 */

FILE_DESCRIPTION(
/* description */ ('PAT-091'),
/* implementation_level */ '2;1');

FILE_NAME(
/* name */ 'Axle distance sleeve 5 mm (10).step',
/* time_stamp */ '2026-10-27T15:34:44-07:00',
/* author */ (''),
/* organization */ (''),
/* preprocessor_version */ 'ST-DEVELOPER v20.2',
/* originating_system */ 'Autodesk Translation Framework v15.17.0.0',
/* authorisation */ '');

FILE_SCHEMA (('AUTOMOTIVE_DESIGN { 1 0 10303 214 3 1 1 }'));
ENDSEC;

DATA;
#10=MECHANICAL_DESIGN_GEOMETRIC_PRESENTATION_REPRESENTATION('',(#1039),#25100);
#819=SHAPE_REPRESENTATION_RELATIONSHIP('SRR','None',#25585,#929);
#929=ADVANCED_BREP_SHAPE_REPRESENTATION('',(#1161),#25055);
#1039=STYLED_ITEM('',(#26191),#1161);
#1161=MANIFOLD_SOLID_BREP('Body1',#13318);
#1516=FACE_BOUND('',#3702,.T.);
#1517=FACE_BOUND('',#3704,.T.);
#1929=PLANE('',#15644);
#1930=PLANE('',#15645);
#2580=FACE_OUTER_BOUND('',#3699,.T.);
#2581=FACE_OUTER_BOUND('',#3700,.T.);
#2582=FACE_OUTER_BOUND('',#3701,.T.);
#2583=FACE_OUTER_BOUND('',#3703,.T.);
#3699=EDGE_LOOP('',(#11032,#11033,#11034,#11035));
#3700=EDGE_LOOP('',(#11036,#11037,#11038,#11039));
#3701=EDGE_LOOP('',(#11040));
#3702=EDGE_LOOP('',(#11041));
#3703=EDGE_LOOP('',(#11042));
#3704=EDGE_LOOP('',(#11043));
#4692=LINE('',#23339,#5432);
#4693=LINE('',#23345,#5433);
#5432=VECTOR('',#19146,0.605);
#5433=VECTOR('',#19153,0.800000000000001);
#6062=CIRCLE('',#15639,0.605);
#6063=CIRCLE('',#15640,0.605);
#6064=CIRCLE('',#15642,0.800000000000001);
#6065=CIRCLE('',#15643,0.800000000000001);
#7067=VERTEX_POINT('',#23336);
#7068=VERTEX_POINT('',#23338);
#7069=VERTEX_POINT('',#23342);
#7070=VERTEX_POINT('',#23344);
#8451=EDGE_CURVE('',#7067,#7067,#6062,.T.);
#8452=EDGE_CURVE('',#7067,#7068,#4692,.T.);
#8453=EDGE_CURVE('',#7068,#7068,#6063,.T.);
#8454=EDGE_CURVE('',#7069,#7069,#6064,.T.);
#8455=EDGE_CURVE('',#7069,#7070,#4693,.T.);
#8456=EDGE_CURVE('',#7070,#7070,#6065,.T.);
#11032=ORIENTED_EDGE('',*,*,#8451,.F.);
#11033=ORIENTED_EDGE('',*,*,#8452,.T.);
#11034=ORIENTED_EDGE('',*,*,#8453,.T.);
#11035=ORIENTED_EDGE('',*,*,#8452,.F.);
#11036=ORIENTED_EDGE('',*,*,#8454,.F.);
#11037=ORIENTED_EDGE('',*,*,#8455,.T.);
#11038=ORIENTED_EDGE('',*,*,#8456,.T.);
#11039=ORIENTED_EDGE('',*,*,#8455,.F.);
#11040=ORIENTED_EDGE('',*,*,#8454,.T.);
#11041=ORIENTED_EDGE('',*,*,#8451,.T.);
#11042=ORIENTED_EDGE('',*,*,#8456,.F.);
#11043=ORIENTED_EDGE('',*,*,#8453,.F.);
#12294=CYLINDRICAL_SURFACE('',#15638,0.605);
#12295=CYLINDRICAL_SURFACE('',#15641,0.800000000000001);
#12947=ADVANCED_FACE('',(#2580),#12294,.F.);
#12948=ADVANCED_FACE('',(#2581),#12295,.T.);
#12949=ADVANCED_FACE('',(#2582,#1516),#1929,.T.);
#12950=ADVANCED_FACE('',(#2583,#1517),#1930,.F.);
#13318=CLOSED_SHELL('',(#12947,#12948,#12949,#12950));
#15637=AXIS2_PLACEMENT_3D('',#23334,#19140,#19141);
#15638=AXIS2_PLACEMENT_3D('',#23335,#19142,#19143);
#15639=AXIS2_PLACEMENT_3D('',#23337,#19144,#19145);
#15640=AXIS2_PLACEMENT_3D('',#23340,#19147,#19148);
#15641=AXIS2_PLACEMENT_3D('',#23341,#19149,#19150);
#15642=AXIS2_PLACEMENT_3D('',#23343,#19151,#19152);
#15643=AXIS2_PLACEMENT_3D('',#23346,#19154,#19155);
#15644=AXIS2_PLACEMENT_3D('',#23347,#19156,#19157);
#15645=AXIS2_PLACEMENT_3D('',#23348,#19158,#19159);
#19140=DIRECTION('axis',(0.,0.,1.));
#19141=DIRECTION('refdir',(1.,0.,0.));
#19142=DIRECTION('center_axis',(0.,1.,0.));
#19143=DIRECTION('ref_axis',(1.,0.,0.));
#19144=DIRECTION('center_axis',(0.,-1.,0.));
#19145=DIRECTION('ref_axis',(1.,0.,0.));
#19146=DIRECTION('',(0.,-1.,0.));
#19147=DIRECTION('center_axis',(0.,-1.,0.));
#19148=DIRECTION('ref_axis',(1.,0.,0.));
#19149=DIRECTION('center_axis',(0.,1.,0.));
#19150=DIRECTION('ref_axis',(1.,0.,0.));
#19151=DIRECTION('center_axis',(0.,1.,0.));
#19152=DIRECTION('ref_axis',(1.,0.,0.));
#19153=DIRECTION('',(0.,-1.,0.));
#19154=DIRECTION('center_axis',(0.,1.,0.));
#19155=DIRECTION('ref_axis',(1.,0.,0.));
#19156=DIRECTION('center_axis',(0.,1.,0.));
#19157=DIRECTION('ref_axis',(1.,0.,0.));
#19158=DIRECTION('center_axis',(0.,1.,0.));
#19159=DIRECTION('ref_axis',(1.,0.,0.));
#23334=CARTESIAN_POINT('',(0.,0.,0.));
#23335=CARTESIAN_POINT('Origin',(19.3649167310371,-6.,8.));
#23336=CARTESIAN_POINT('',(18.7599167310371,-5.5,8.));
#23337=CARTESIAN_POINT('Origin',(19.3649167310371,-5.5,8.));
#23338=CARTESIAN_POINT('',(18.7599167310371,-6.,8.));
#23339=CARTESIAN_POINT('',(18.7599167310371,-6.,8.));
#23340=CARTESIAN_POINT('Origin',(19.3649167310371,-6.,8.));
#23341=CARTESIAN_POINT('Origin',(19.3649167310371,-6.,8.));
#23342=CARTESIAN_POINT('',(18.5649167310371,-5.5,8.));
#23343=CARTESIAN_POINT('Origin',(19.3649167310371,-5.5,8.));
#23344=CARTESIAN_POINT('',(18.5649167310371,-6.,8.));
#23345=CARTESIAN_POINT('',(18.5649167310371,-6.,8.));
#23346=CARTESIAN_POINT('Origin',(19.3649167310371,-6.,8.));
#23347=CARTESIAN_POINT('Origin',(19.3649167310371,-5.5,8.));
#23348=CARTESIAN_POINT('Origin',(19.3649167310371,-6.,8.));
#24934=UNCERTAINTY_MEASURE_WITH_UNIT(LENGTH_MEASURE(0.001),#25101,
'DISTANCE_ACCURACY_VALUE',
'Maximum model space distance between geometric entities at asserted c
onnectivities');
#24979=UNCERTAINTY_MEASURE_WITH_UNIT(LENGTH_MEASURE(0.001),#25101,
'DISTANCE_ACCURACY_VALUE',
'Maximum model space distance between geometric entities at asserted c
onnectivities');
#25055=(
GEOMETRIC_REPRESENTATION_CONTEXT(3)
GLOBAL_UNCERTAINTY_ASSIGNED_CONTEXT((#24934))
GLOBAL_UNIT_ASSIGNED_CONTEXT((#25101,#25103,#25104))
REPRESENTATION_CONTEXT('','3D')
);
#25100=(
GEOMETRIC_REPRESENTATION_CONTEXT(3)
GLOBAL_UNCERTAINTY_ASSIGNED_CONTEXT((#24979))
GLOBAL_UNIT_ASSIGNED_CONTEXT((#25101,#25103,#25104))
REPRESENTATION_CONTEXT('','3D')
);
#25101=(
LENGTH_UNIT()
NAMED_UNIT(*)
SI_UNIT(.CENTI.,.METRE.)
);
#25103=(
NAMED_UNIT(*)
PLANE_ANGLE_UNIT()
SI_UNIT($,.RADIAN.)
);
#25104=(
NAMED_UNIT(*)
SI_UNIT($,.STERADIAN.)
SOLID_ANGLE_UNIT()
);
#25180=SHAPE_DEFINITION_REPRESENTATION(#25302,#25585);
#25302=PRODUCT_DEFINITION_SHAPE('',$,#25706);
#25585=SHAPE_REPRESENTATION('',(#15637),#25055);
#25630=PRODUCT_DEFINITION_CONTEXT('part definition',#25992,'design');
#25706=PRODUCT_DEFINITION('Axle distance sleeve 5 mm (10)',
'Axle distance sleeve 5 mm (10)',#25826,#25630);
#25826=PRODUCT_DEFINITION_FORMATION('',$,#26069);
#25992=APPLICATION_CONTEXT(
'Core Data for Automotive Mechanical Design Process');
#25993=PRODUCT_CONTEXT('part definition',#25992,'mechanical');
#26069=PRODUCT('Axle distance sleeve 5 mm (10)',
'Axle distance sleeve 5 mm (10)','Axle distance sleeve 5 mm (10)',(#25993));
#26185=COLOUR_RGB('Grey',0.48,0.52,0.57);
#26186=FILL_AREA_STYLE_COLOUR('',#26185);
#26187=FILL_AREA_STYLE('',(#26186));
#26188=SURFACE_STYLE_FILL_AREA(#26187);
#26189=SURFACE_SIDE_STYLE('',(#26188));
#26190=SURFACE_STYLE_USAGE(.BOTH.,#26189);
#26191=PRESENTATION_STYLE_ASSIGNMENT((#26190));
ENDSEC;
END-ISO-10303-21;
